ISO-10303-21;
HEADER;
/* Generated by software containing ST-Developer
 * from STEP Tools, Inc. (www.steptools.com) 
 */

FILE_DESCRIPTION(
/* description */ ('Independent four-jaw lathe chuck,200mm body,40mm bore,36\X2\2013\X0\7
6mm nominal opposed jaw opening. Four shared machined T-jaws and model
ed partial M12x1.75 feed screws, native independent screw/slider links
, removable bolted bronze-bearing cartridges, fully captured ring/wash
er/head thrust stacks and registered bolted backplate. Custom spindle 
interface; no compatibility, speed, grip force or safety rating assign
ed.'),
/* implementation_level */ '2;1');

FILE_NAME(
/* name */ 'Washer M6.step',
/* time_stamp */ '2026-11-09T20:24:54-08:00',
/* author */ (''),
/* organization */ (''),
/* preprocessor_version */ 'ST-DEVELOPER v20.2',
/* originating_system */ 'Autodesk Translation Framework v15.17.0.0',
/* authorisation */ '');

FILE_SCHEMA (('AUTOMOTIVE_DESIGN { 1 0 10303 214 3 1 1 }'));
ENDSEC;

DATA;
#10=MECHANICAL_DESIGN_GEOMETRIC_PRESENTATION_REPRESENTATION('',(#245),#69491);
#223=SHAPE_REPRESENTATION_RELATIONSHIP('SRR','None',#69580,#234);
#234=ADVANCED_BREP_SHAPE_REPRESENTATION('',(#256),#69489);
#245=STYLED_ITEM('',(#69643),#256);
#256=MANIFOLD_SOLID_BREP('Body1',#14740);
#361=FACE_BOUND('',#2065,.T.);
#362=FACE_BOUND('',#2067,.T.);
#510=PLANE('',#15722);
#511=PLANE('',#15723);
#1218=FACE_OUTER_BOUND('',#2062,.T.);
#1219=FACE_OUTER_BOUND('',#2063,.T.);
#1220=FACE_OUTER_BOUND('',#2064,.T.);
#1221=FACE_OUTER_BOUND('',#2066,.T.);
#2062=EDGE_LOOP('',(#12899,#12900,#12901,#12902));
#2063=EDGE_LOOP('',(#12903,#12904,#12905,#12906));
#2064=EDGE_LOOP('',(#12907));
#2065=EDGE_LOOP('',(#12908));
#2066=EDGE_LOOP('',(#12909));
#2067=EDGE_LOOP('',(#12910));
#2334=CIRCLE('',#15717,3.5);
#2335=CIRCLE('',#15718,3.5);
#2336=CIRCLE('',#15720,7.);
#2337=CIRCLE('',#15721,7.);
#4288=LINE('',#64819,#5136);
#4289=LINE('',#64825,#5137);
#5136=VECTOR('',#18332,3.5);
#5137=VECTOR('',#18339,7.);
#6541=VERTEX_POINT('',#64816);
#6542=VERTEX_POINT('',#64818);
#6543=VERTEX_POINT('',#64822);
#6544=VERTEX_POINT('',#64824);
#8686=EDGE_CURVE('',#6541,#6541,#2334,.T.);
#8687=EDGE_CURVE('',#6541,#6542,#4288,.T.);
#8688=EDGE_CURVE('',#6542,#6542,#2335,.T.);
#8689=EDGE_CURVE('',#6543,#6543,#2336,.T.);
#8690=EDGE_CURVE('',#6543,#6544,#4289,.T.);
#8691=EDGE_CURVE('',#6544,#6544,#2337,.T.);
#12899=ORIENTED_EDGE('',*,*,#8686,.F.);
#12900=ORIENTED_EDGE('',*,*,#8687,.T.);
#12901=ORIENTED_EDGE('',*,*,#8688,.T.);
#12902=ORIENTED_EDGE('',*,*,#8687,.F.);
#12903=ORIENTED_EDGE('',*,*,#8689,.F.);
#12904=ORIENTED_EDGE('',*,*,#8690,.T.);
#12905=ORIENTED_EDGE('',*,*,#8691,.T.);
#12906=ORIENTED_EDGE('',*,*,#8690,.F.);
#12907=ORIENTED_EDGE('',*,*,#8689,.T.);
#12908=ORIENTED_EDGE('',*,*,#8686,.T.);
#12909=ORIENTED_EDGE('',*,*,#8691,.F.);
#12910=ORIENTED_EDGE('',*,*,#8688,.F.);
#13881=CYLINDRICAL_SURFACE('',#15716,3.5);
#13882=CYLINDRICAL_SURFACE('',#15719,7.);
#14646=ADVANCED_FACE('',(#1218),#13881,.F.);
#14647=ADVANCED_FACE('',(#1219),#13882,.T.);
#14648=ADVANCED_FACE('',(#1220,#361),#510,.T.);
#14649=ADVANCED_FACE('',(#1221,#362),#511,.F.);
#14740=CLOSED_SHELL('',(#14646,#14647,#14648,#14649));
#15715=AXIS2_PLACEMENT_3D('',#64814,#18326,#18327);
#15716=AXIS2_PLACEMENT_3D('',#64815,#18328,#18329);
#15717=AXIS2_PLACEMENT_3D('',#64817,#18330,#18331);
#15718=AXIS2_PLACEMENT_3D('',#64820,#18333,#18334);
#15719=AXIS2_PLACEMENT_3D('',#64821,#18335,#18336);
#15720=AXIS2_PLACEMENT_3D('',#64823,#18337,#18338);
#15721=AXIS2_PLACEMENT_3D('',#64826,#18340,#18341);
#15722=AXIS2_PLACEMENT_3D('',#64827,#18342,#18343);
#15723=AXIS2_PLACEMENT_3D('',#64828,#18344,#18345);
#18326=DIRECTION('axis',(0.,0.,1.));
#18327=DIRECTION('refdir',(1.,0.,0.));
#18328=DIRECTION('center_axis',(0.,0.,1.));
#18329=DIRECTION('ref_axis',(1.,0.,0.));
#18330=DIRECTION('center_axis',(0.,0.,-1.));
#18331=DIRECTION('ref_axis',(1.,0.,0.));
#18332=DIRECTION('',(0.,0.,-1.));
#18333=DIRECTION('center_axis',(0.,0.,-1.));
#18334=DIRECTION('ref_axis',(1.,0.,0.));
#18335=DIRECTION('center_axis',(0.,0.,1.));
#18336=DIRECTION('ref_axis',(1.,0.,0.));
#18337=DIRECTION('center_axis',(0.,0.,1.));
#18338=DIRECTION('ref_axis',(1.,0.,0.));
#18339=DIRECTION('',(0.,0.,-1.));
#18340=DIRECTION('center_axis',(0.,0.,1.));
#18341=DIRECTION('ref_axis',(1.,0.,0.));
#18342=DIRECTION('center_axis',(0.,0.,1.));
#18343=DIRECTION('ref_axis',(1.,0.,0.));
#18344=DIRECTION('center_axis',(0.,0.,1.));
#18345=DIRECTION('ref_axis',(1.,0.,0.));
#64814=CARTESIAN_POINT('',(0.,0.,0.));
#64815=CARTESIAN_POINT('Origin',(0.,0.,0.));
#64816=CARTESIAN_POINT('',(-3.5,-4.28626379701574E-16,2.));
#64817=CARTESIAN_POINT('Origin',(0.,0.,2.));
#64818=CARTESIAN_POINT('',(-3.5,-4.28626379701574E-16,0.));
#64819=CARTESIAN_POINT('',(-3.5,-4.28626379701574E-16,0.));
#64820=CARTESIAN_POINT('Origin',(0.,0.,0.));
#64821=CARTESIAN_POINT('Origin',(0.,0.,0.));
#64822=CARTESIAN_POINT('',(-7.,-8.57252759403147E-16,2.));
#64823=CARTESIAN_POINT('Origin',(0.,0.,2.));
#64824=CARTESIAN_POINT('',(-7.,-8.57252759403147E-16,0.));
#64825=CARTESIAN_POINT('',(-7.,-8.57252759403147E-16,0.));
#64826=CARTESIAN_POINT('Origin',(0.,0.,0.));
#64827=CARTESIAN_POINT('Origin',(0.,0.,2.));
#64828=CARTESIAN_POINT('Origin',(0.,0.,0.));
#69476=UNCERTAINTY_MEASURE_WITH_UNIT(LENGTH_MEASURE(0.01),#69492,
'DISTANCE_ACCURACY_VALUE',
'Maximum model space distance between geometric entities at asserted c
onnectivities');
#69478=UNCERTAINTY_MEASURE_WITH_UNIT(LENGTH_MEASURE(0.01),#69492,
'DISTANCE_ACCURACY_VALUE',
'Maximum model space distance between geometric entities at asserted c
onnectivities');
#69489=(
GEOMETRIC_REPRESENTATION_CONTEXT(3)
GLOBAL_UNCERTAINTY_ASSIGNED_CONTEXT((#69476))
GLOBAL_UNIT_ASSIGNED_CONTEXT((#69492,#69494,#69495))
REPRESENTATION_CONTEXT('','3D')
);
#69491=(
GEOMETRIC_REPRESENTATION_CONTEXT(3)
GLOBAL_UNCERTAINTY_ASSIGNED_CONTEXT((#69478))
GLOBAL_UNIT_ASSIGNED_CONTEXT((#69492,#69494,#69495))
REPRESENTATION_CONTEXT('','3D')
);
#69492=(
LENGTH_UNIT()
NAMED_UNIT(*)
SI_UNIT(.MILLI.,.METRE.)
);
#69494=(
NAMED_UNIT(*)
PLANE_ANGLE_UNIT()
SI_UNIT($,.RADIAN.)
);
#69495=(
NAMED_UNIT(*)
SI_UNIT($,.STERADIAN.)
SOLID_ANGLE_UNIT()
);
#69506=SHAPE_DEFINITION_REPRESENTATION(#69518,#69580);
#69518=PRODUCT_DEFINITION_SHAPE('',$,#69593);
#69580=SHAPE_REPRESENTATION('',(#15715),#69489);
#69582=PRODUCT_DEFINITION_CONTEXT('part definition',#69620,'design');
#69593=PRODUCT_DEFINITION('Washer M6','Washer M6',#69605,#69582);
#69605=PRODUCT_DEFINITION_FORMATION('',$,#69632);
#69620=APPLICATION_CONTEXT(
'Core Data for Automotive Mechanical Design Process');
#69621=PRODUCT_CONTEXT('part definition',#69620,'mechanical');
#69632=PRODUCT('Washer M6','Washer M6',$,(#69621));
#69643=PRESENTATION_STYLE_ASSIGNMENT((#69653));
#69653=SURFACE_STYLE_USAGE(.BOTH.,#69663);
#69663=SURFACE_SIDE_STYLE('',(#69673));
#69673=SURFACE_STYLE_FILL_AREA(#69683);
#69683=FILL_AREA_STYLE('Light gray',(#69693));
#69693=FILL_AREA_STYLE_COLOUR('Light gray',#69703);
#69703=COLOUR_RGB('Light gray',0.725490196078431,0.752941176470588,0.792156862745098);
ENDSEC;
END-ISO-10303-21;
